ISO-10303-21;
HEADER;
/* Generated by software containing ST-Developer
 * from STEP Tools, Inc. (www.steptools.com) 
 */

FILE_DESCRIPTION(
/* description */ ('Line shaft on three pillow blocks'),
/* implementation_level */ '2;1');

FILE_NAME(
/* name */ 'Cross foot (1).step',
/* time_stamp */ '2026-10-27T10:49:19-07:00',
/* author */ (''),
/* organization */ (''),
/* preprocessor_version */ 'ST-DEVELOPER v20.2',
/* originating_system */ 'Autodesk Translation Framework v15.17.0.0',
/* authorisation */ '');

FILE_SCHEMA (('AUTOMOTIVE_DESIGN { 1 0 10303 214 3 1 1 }'));
ENDSEC;

DATA;
#10=MECHANICAL_DESIGN_GEOMETRIC_PRESENTATION_REPRESENTATION('',(#341),#8377);
#287=SHAPE_REPRESENTATION_RELATIONSHIP('SRR','None',#8502,#314);
#314=ADVANCED_BREP_SHAPE_REPRESENTATION('',(#369),#8351);
#341=STYLED_ITEM('',(#8732),#369);
#369=MANIFOLD_SOLID_BREP('Body1',#4327);
#413=FACE_BOUND('',#969,.T.);
#414=FACE_BOUND('',#970,.T.);
#508=PLANE('',#4718);
#509=PLANE('',#4722);
#510=PLANE('',#4723);
#511=PLANE('',#4724);
#512=PLANE('',#4725);
#513=PLANE('',#4726);
#514=PLANE('',#4727);
#515=PLANE('',#4728);
#686=FACE_OUTER_BOUND('',#960,.T.);
#687=FACE_OUTER_BOUND('',#961,.T.);
#688=FACE_OUTER_BOUND('',#962,.T.);
#689=FACE_OUTER_BOUND('',#963,.T.);
#690=FACE_OUTER_BOUND('',#964,.T.);
#691=FACE_OUTER_BOUND('',#965,.T.);
#692=FACE_OUTER_BOUND('',#966,.T.);
#693=FACE_OUTER_BOUND('',#967,.T.);
#694=FACE_OUTER_BOUND('',#968,.T.);
#695=FACE_OUTER_BOUND('',#971,.T.);
#960=EDGE_LOOP('',(#3093,#3094,#3095,#3096));
#961=EDGE_LOOP('',(#3097));
#962=EDGE_LOOP('',(#3098,#3099,#3100,#3101));
#963=EDGE_LOOP('',(#3102));
#964=EDGE_LOOP('',(#3103,#3104,#3105,#3106));
#965=EDGE_LOOP('',(#3107,#3108,#3109,#3110));
#966=EDGE_LOOP('',(#3111,#3112,#3113,#3114));
#967=EDGE_LOOP('',(#3115,#3116,#3117,#3118));
#968=EDGE_LOOP('',(#3119,#3120,#3121,#3122));
#969=EDGE_LOOP('',(#3123));
#970=EDGE_LOOP('',(#3124));
#971=EDGE_LOOP('',(#3125,#3126,#3127,#3128));
#1303=LINE('',#6627,#1630);
#1304=LINE('',#6634,#1631);
#1305=LINE('',#6640,#1632);
#1306=LINE('',#6642,#1633);
#1307=LINE('',#6644,#1634);
#1308=LINE('',#6645,#1635);
#1309=LINE('',#6648,#1636);
#1310=LINE('',#6650,#1637);
#1311=LINE('',#6651,#1638);
#1312=LINE('',#6654,#1639);
#1313=LINE('',#6656,#1640);
#1314=LINE('',#6657,#1641);
#1315=LINE('',#6659,#1642);
#1316=LINE('',#6660,#1643);
#1630=VECTOR('',#5324,0.25);
#1631=VECTOR('',#5333,0.25);
#1632=VECTOR('',#5340,1.);
#1633=VECTOR('',#5341,1.);
#1634=VECTOR('',#5342,1.);
#1635=VECTOR('',#5343,1.);
#1636=VECTOR('',#5346,1.);
#1637=VECTOR('',#5347,1.);
#1638=VECTOR('',#5348,1.);
#1639=VECTOR('',#5351,1.);
#1640=VECTOR('',#5352,1.);
#1641=VECTOR('',#5353,1.);
#1642=VECTOR('',#5356,1.);
#1643=VECTOR('',#5357,1.);
#1933=CIRCLE('',#4716,0.25);
#1934=CIRCLE('',#4717,0.25);
#1935=CIRCLE('',#4720,0.25);
#1936=CIRCLE('',#4721,0.25);
#2116=VERTEX_POINT('',#6624);
#2117=VERTEX_POINT('',#6626);
#2118=VERTEX_POINT('',#6631);
#2119=VERTEX_POINT('',#6633);
#2120=VERTEX_POINT('',#6638);
#2121=VERTEX_POINT('',#6639);
#2122=VERTEX_POINT('',#6641);
#2123=VERTEX_POINT('',#6643);
#2124=VERTEX_POINT('',#6647);
#2125=VERTEX_POINT('',#6649);
#2126=VERTEX_POINT('',#6653);
#2127=VERTEX_POINT('',#6655);
#2495=EDGE_CURVE('',#2116,#2116,#1933,.T.);
#2496=EDGE_CURVE('',#2116,#2117,#1303,.T.);
#2497=EDGE_CURVE('',#2117,#2117,#1934,.T.);
#2498=EDGE_CURVE('',#2118,#2118,#1935,.T.);
#2499=EDGE_CURVE('',#2118,#2119,#1304,.T.);
#2500=EDGE_CURVE('',#2119,#2119,#1936,.T.);
#2501=EDGE_CURVE('',#2120,#2121,#1305,.T.);
#2502=EDGE_CURVE('',#2121,#2122,#1306,.T.);
#2503=EDGE_CURVE('',#2123,#2122,#1307,.T.);
#2504=EDGE_CURVE('',#2120,#2123,#1308,.T.);
#2505=EDGE_CURVE('',#2124,#2120,#1309,.T.);
#2506=EDGE_CURVE('',#2125,#2123,#1310,.T.);
#2507=EDGE_CURVE('',#2124,#2125,#1311,.T.);
#2508=EDGE_CURVE('',#2126,#2124,#1312,.T.);
#2509=EDGE_CURVE('',#2127,#2125,#1313,.T.);
#2510=EDGE_CURVE('',#2126,#2127,#1314,.T.);
#2511=EDGE_CURVE('',#2121,#2126,#1315,.T.);
#2512=EDGE_CURVE('',#2122,#2127,#1316,.T.);
#3093=ORIENTED_EDGE('',*,*,#2495,.F.);
#3094=ORIENTED_EDGE('',*,*,#2496,.T.);
#3095=ORIENTED_EDGE('',*,*,#2497,.F.);
#3096=ORIENTED_EDGE('',*,*,#2496,.F.);
#3097=ORIENTED_EDGE('',*,*,#2495,.T.);
#3098=ORIENTED_EDGE('',*,*,#2498,.F.);
#3099=ORIENTED_EDGE('',*,*,#2499,.T.);
#3100=ORIENTED_EDGE('',*,*,#2500,.F.);
#3101=ORIENTED_EDGE('',*,*,#2499,.F.);
#3102=ORIENTED_EDGE('',*,*,#2498,.T.);
#3103=ORIENTED_EDGE('',*,*,#2501,.T.);
#3104=ORIENTED_EDGE('',*,*,#2502,.T.);
#3105=ORIENTED_EDGE('',*,*,#2503,.F.);
#3106=ORIENTED_EDGE('',*,*,#2504,.F.);
#3107=ORIENTED_EDGE('',*,*,#2505,.T.);
#3108=ORIENTED_EDGE('',*,*,#2504,.T.);
#3109=ORIENTED_EDGE('',*,*,#2506,.F.);
#3110=ORIENTED_EDGE('',*,*,#2507,.F.);
#3111=ORIENTED_EDGE('',*,*,#2508,.T.);
#3112=ORIENTED_EDGE('',*,*,#2507,.T.);
#3113=ORIENTED_EDGE('',*,*,#2509,.F.);
#3114=ORIENTED_EDGE('',*,*,#2510,.F.);
#3115=ORIENTED_EDGE('',*,*,#2511,.T.);
#3116=ORIENTED_EDGE('',*,*,#2510,.T.);
#3117=ORIENTED_EDGE('',*,*,#2512,.F.);
#3118=ORIENTED_EDGE('',*,*,#2502,.F.);
#3119=ORIENTED_EDGE('',*,*,#2512,.T.);
#3120=ORIENTED_EDGE('',*,*,#2509,.T.);
#3121=ORIENTED_EDGE('',*,*,#2506,.T.);
#3122=ORIENTED_EDGE('',*,*,#2503,.T.);
#3123=ORIENTED_EDGE('',*,*,#2497,.T.);
#3124=ORIENTED_EDGE('',*,*,#2500,.T.);
#3125=ORIENTED_EDGE('',*,*,#2511,.F.);
#3126=ORIENTED_EDGE('',*,*,#2501,.F.);
#3127=ORIENTED_EDGE('',*,*,#2505,.F.);
#3128=ORIENTED_EDGE('',*,*,#2508,.F.);
#4013=CYLINDRICAL_SURFACE('',#4715,0.25);
#4014=CYLINDRICAL_SURFACE('',#4719,0.25);
#4104=ADVANCED_FACE('',(#686),#4013,.F.);
#4105=ADVANCED_FACE('',(#687),#508,.T.);
#4106=ADVANCED_FACE('',(#688),#4014,.F.);
#4107=ADVANCED_FACE('',(#689),#509,.T.);
#4108=ADVANCED_FACE('',(#690),#510,.T.);
#4109=ADVANCED_FACE('',(#691),#511,.T.);
#4110=ADVANCED_FACE('',(#692),#512,.T.);
#4111=ADVANCED_FACE('',(#693),#513,.T.);
#4112=ADVANCED_FACE('',(#694,#413,#414),#514,.T.);
#4113=ADVANCED_FACE('',(#695),#515,.F.);
#4327=CLOSED_SHELL('',(#4104,#4105,#4106,#4107,#4108,#4109,#4110,#4111,
#4112,#4113));
#4714=AXIS2_PLACEMENT_3D('',#6622,#5318,#5319);
#4715=AXIS2_PLACEMENT_3D('',#6623,#5320,#5321);
#4716=AXIS2_PLACEMENT_3D('',#6625,#5322,#5323);
#4717=AXIS2_PLACEMENT_3D('',#6628,#5325,#5326);
#4718=AXIS2_PLACEMENT_3D('',#6629,#5327,#5328);
#4719=AXIS2_PLACEMENT_3D('',#6630,#5329,#5330);
#4720=AXIS2_PLACEMENT_3D('',#6632,#5331,#5332);
#4721=AXIS2_PLACEMENT_3D('',#6635,#5334,#5335);
#4722=AXIS2_PLACEMENT_3D('',#6636,#5336,#5337);
#4723=AXIS2_PLACEMENT_3D('',#6637,#5338,#5339);
#4724=AXIS2_PLACEMENT_3D('',#6646,#5344,#5345);
#4725=AXIS2_PLACEMENT_3D('',#6652,#5349,#5350);
#4726=AXIS2_PLACEMENT_3D('',#6658,#5354,#5355);
#4727=AXIS2_PLACEMENT_3D('',#6661,#5358,#5359);
#4728=AXIS2_PLACEMENT_3D('',#6662,#5360,#5361);
#5318=DIRECTION('axis',(0.,0.,1.));
#5319=DIRECTION('refdir',(1.,0.,0.));
#5320=DIRECTION('center_axis',(0.,0.,1.));
#5321=DIRECTION('ref_axis',(1.,0.,0.));
#5322=DIRECTION('center_axis',(0.,0.,1.));
#5323=DIRECTION('ref_axis',(1.,0.,0.));
#5324=DIRECTION('',(0.,0.,1.));
#5325=DIRECTION('center_axis',(0.,0.,-1.));
#5326=DIRECTION('ref_axis',(1.,0.,0.));
#5327=DIRECTION('center_axis',(0.,0.,1.));
#5328=DIRECTION('ref_axis',(1.,0.,0.));
#5329=DIRECTION('center_axis',(0.,0.,1.));
#5330=DIRECTION('ref_axis',(1.,0.,0.));
#5331=DIRECTION('center_axis',(0.,0.,1.));
#5332=DIRECTION('ref_axis',(1.,0.,0.));
#5333=DIRECTION('',(0.,0.,1.));
#5334=DIRECTION('center_axis',(0.,0.,-1.));
#5335=DIRECTION('ref_axis',(1.,0.,0.));
#5336=DIRECTION('center_axis',(0.,0.,1.));
#5337=DIRECTION('ref_axis',(1.,0.,0.));
#5338=DIRECTION('center_axis',(0.,1.,0.));
#5339=DIRECTION('ref_axis',(-1.,0.,0.));
#5340=DIRECTION('',(-1.,0.,0.));
#5341=DIRECTION('',(0.,0.,1.));
#5342=DIRECTION('',(-1.,0.,0.));
#5343=DIRECTION('',(0.,0.,1.));
#5344=DIRECTION('center_axis',(1.,0.,0.));
#5345=DIRECTION('ref_axis',(0.,1.,0.));
#5346=DIRECTION('',(0.,1.,0.));
#5347=DIRECTION('',(0.,1.,0.));
#5348=DIRECTION('',(0.,0.,1.));
#5349=DIRECTION('center_axis',(0.,-1.,0.));
#5350=DIRECTION('ref_axis',(1.,0.,0.));
#5351=DIRECTION('',(1.,0.,0.));
#5352=DIRECTION('',(1.,0.,0.));
#5353=DIRECTION('',(0.,0.,1.));
#5354=DIRECTION('center_axis',(-1.,0.,0.));
#5355=DIRECTION('ref_axis',(0.,-1.,0.));
#5356=DIRECTION('',(0.,-1.,0.));
#5357=DIRECTION('',(0.,-1.,0.));
#5358=DIRECTION('center_axis',(0.,0.,1.));
#5359=DIRECTION('ref_axis',(1.,0.,0.));
#5360=DIRECTION('center_axis',(0.,0.,1.));
#5361=DIRECTION('ref_axis',(1.,0.,0.));
#6622=CARTESIAN_POINT('',(0.,0.,0.));
#6623=CARTESIAN_POINT('Origin',(-6.,33.,-1.3));
#6624=CARTESIAN_POINT('',(-6.25,33.,-1.3));
#6625=CARTESIAN_POINT('Origin',(-6.,33.,-1.3));
#6626=CARTESIAN_POINT('',(-6.25,33.,0.));
#6627=CARTESIAN_POINT('',(-6.25,33.,-1.3));
#6628=CARTESIAN_POINT('Origin',(-6.,33.,0.));
#6629=CARTESIAN_POINT('Origin',(-6.,33.,-1.3));
#6630=CARTESIAN_POINT('Origin',(6.,33.,-1.3));
#6631=CARTESIAN_POINT('',(5.75,33.,-1.3));
#6632=CARTESIAN_POINT('Origin',(6.,33.,-1.3));
#6633=CARTESIAN_POINT('',(5.75,33.,0.));
#6634=CARTESIAN_POINT('',(5.75,33.,-1.3));
#6635=CARTESIAN_POINT('Origin',(6.,33.,0.));
#6636=CARTESIAN_POINT('Origin',(6.,33.,-1.3));
#6637=CARTESIAN_POINT('Origin',(9.,34.,-1.5));
#6638=CARTESIAN_POINT('',(9.,34.,-1.5));
#6639=CARTESIAN_POINT('',(-9.,34.,-1.5));
#6640=CARTESIAN_POINT('',(9.,34.,-1.5));
#6641=CARTESIAN_POINT('',(-9.,34.,0.));
#6642=CARTESIAN_POINT('',(-9.,34.,-1.5));
#6643=CARTESIAN_POINT('',(9.,34.,0.));
#6644=CARTESIAN_POINT('',(9.,34.,0.));
#6645=CARTESIAN_POINT('',(9.,34.,-1.5));
#6646=CARTESIAN_POINT('Origin',(9.,32.,-1.5));
#6647=CARTESIAN_POINT('',(9.,32.,-1.5));
#6648=CARTESIAN_POINT('',(9.,32.,-1.5));
#6649=CARTESIAN_POINT('',(9.,32.,0.));
#6650=CARTESIAN_POINT('',(9.,32.,0.));
#6651=CARTESIAN_POINT('',(9.,32.,-1.5));
#6652=CARTESIAN_POINT('Origin',(-9.,32.,-1.5));
#6653=CARTESIAN_POINT('',(-9.,32.,-1.5));
#6654=CARTESIAN_POINT('',(-9.,32.,-1.5));
#6655=CARTESIAN_POINT('',(-9.,32.,0.));
#6656=CARTESIAN_POINT('',(-9.,32.,0.));
#6657=CARTESIAN_POINT('',(-9.,32.,-1.5));
#6658=CARTESIAN_POINT('Origin',(-9.,34.,-1.5));
#6659=CARTESIAN_POINT('',(-9.,34.,-1.5));
#6660=CARTESIAN_POINT('',(-9.,34.,0.));
#6661=CARTESIAN_POINT('Origin',(0.,33.,0.));
#6662=CARTESIAN_POINT('Origin',(0.,33.,-1.5));
#8319=UNCERTAINTY_MEASURE_WITH_UNIT(LENGTH_MEASURE(0.001),#8378,
'DISTANCE_ACCURACY_VALUE',
'Maximum model space distance between geometric entities at asserted c
onnectivities');
#8345=UNCERTAINTY_MEASURE_WITH_UNIT(LENGTH_MEASURE(0.001),#8378,
'DISTANCE_ACCURACY_VALUE',
'Maximum model space distance between geometric entities at asserted c
onnectivities');
#8351=(
GEOMETRIC_REPRESENTATION_CONTEXT(3)
GLOBAL_UNCERTAINTY_ASSIGNED_CONTEXT((#8319))
GLOBAL_UNIT_ASSIGNED_CONTEXT((#8378,#8380,#8381))
REPRESENTATION_CONTEXT('','3D')
);
#8377=(
GEOMETRIC_REPRESENTATION_CONTEXT(3)
GLOBAL_UNCERTAINTY_ASSIGNED_CONTEXT((#8345))
GLOBAL_UNIT_ASSIGNED_CONTEXT((#8378,#8380,#8381))
REPRESENTATION_CONTEXT('','3D')
);
#8378=(
LENGTH_UNIT()
NAMED_UNIT(*)
SI_UNIT(.CENTI.,.METRE.)
);
#8380=(
NAMED_UNIT(*)
PLANE_ANGLE_UNIT()
SI_UNIT($,.RADIAN.)
);
#8381=(
NAMED_UNIT(*)
SI_UNIT($,.STERADIAN.)
SOLID_ANGLE_UNIT()
);
#8387=SHAPE_DEFINITION_REPRESENTATION(#8418,#8502);
#8418=PRODUCT_DEFINITION_SHAPE('',$,#8534);
#8502=SHAPE_REPRESENTATION('',(#4714),#8351);
#8528=PRODUCT_DEFINITION_CONTEXT('part definition',#8623,'design');
#8534=PRODUCT_DEFINITION('Cross foot (1)','Cross foot (1)',#8565,#8528);
#8565=PRODUCT_DEFINITION_FORMATION('',$,#8630);
#8623=APPLICATION_CONTEXT(
'Core Data for Automotive Mechanical Design Process');
#8624=PRODUCT_CONTEXT('part definition',#8623,'mechanical');
#8630=PRODUCT('Cross foot (1)','Cross foot (1)','Cross foot (1)',(#8624));
#8726=COLOUR_RGB('Off White',0.89,0.88,0.83);
#8727=FILL_AREA_STYLE_COLOUR('',#8726);
#8728=FILL_AREA_STYLE('',(#8727));
#8729=SURFACE_STYLE_FILL_AREA(#8728);
#8730=SURFACE_SIDE_STYLE('',(#8729));
#8731=SURFACE_STYLE_USAGE(.BOTH.,#8730);
#8732=PRESENTATION_STYLE_ASSIGNMENT((#8731));
ENDSEC;
END-ISO-10303-21;
